ISO-10303-21;
HEADER;
/* Generated by software containing ST-Developer
 * from STEP Tools, Inc. (www.steptools.com) 
 */
/* OPTION: using custom renumber hook */

FILE_DESCRIPTION(
/* description */ ('STEP AP242 Edition 2', 'CAx-IF Rec.Pracs.---Representation and Presentation of Product Manufa
cturing Information (PMI)---4.0---2014-10-13', 'CAx-IF Rec.Pracs.---3D Tessellated Geometry---0.4---2014-09-14', '2;1', 'CAx-IF Rec.Pracs.---User Defined Attributes---1.5---2016-08-15'),
/* implementation_level */ '2;1');

FILE_NAME(
/* name */ 'Part 1__PD8593.step',
/* time_stamp */ '2026-10-07T00:00:55Z',
/* author */ (''),
/* organization */ (''),
/* preprocessor_version */ 'ST-DEVELOPER v20',
/* originating_system */ 'ONSHAPE BY PTC INC, 1.221',
/* authorisation */ '  ');

FILE_SCHEMA (('AP242_MANAGED_MODEL_BASED_3D_ENGINEERING_MIM_LF { 1 0 10303 442 3 1 4 }'));
ENDSEC;

DATA;
#120=SHAPE_REPRESENTATION_RELATIONSHIP('','',#4476,#131);
#131=ADVANCED_BREP_SHAPE_REPRESENTATION('',(#4452),#8539);
#209=CYLINDRICAL_SURFACE('',#4534,0.01);
#210=CYLINDRICAL_SURFACE('',#4536,0.038727);
#211=CYLINDRICAL_SURFACE('',#4539,0.0294270007);
#212=CYLINDRICAL_SURFACE('',#4544,0.038727);
#213=CYLINDRICAL_SURFACE('',#4548,0.03442700038);
#214=CYLINDRICAL_SURFACE('',#4552,0.038727);
#215=CYLINDRICAL_SURFACE('',#4556,0.03442700038);
#216=CYLINDRICAL_SURFACE('',#4560,0.038727);
#217=CYLINDRICAL_SURFACE('',#4564,0.03442700038);
#218=CYLINDRICAL_SURFACE('',#4568,0.038727);
#219=CYLINDRICAL_SURFACE('',#4572,0.0344270003800001);
#220=CYLINDRICAL_SURFACE('',#4577,0.014);
#221=CYLINDRICAL_SURFACE('',#4580,0.014);
#222=CYLINDRICAL_SURFACE('',#4584,0.01);
#326=CIRCLE('',#4535,0.01);
#327=CIRCLE('',#4537,0.038727);
#328=CIRCLE('',#4538,0.038727);
#329=CIRCLE('',#4540,0.0294270007);
#330=CIRCLE('',#4541,0.0294270007);
#331=CIRCLE('',#4543,0.038727);
#332=CIRCLE('',#4545,0.038727);
#333=CIRCLE('',#4547,0.03442700038);
#334=CIRCLE('',#4549,0.03442700038);
#335=CIRCLE('',#4551,0.038727);
#336=CIRCLE('',#4553,0.038727);
#337=CIRCLE('',#4555,0.03442700038);
#338=CIRCLE('',#4557,0.03442700038);
#339=CIRCLE('',#4559,0.038727);
#340=CIRCLE('',#4561,0.038727);
#341=CIRCLE('',#4563,0.03442700038);
#342=CIRCLE('',#4565,0.03442700038);
#343=CIRCLE('',#4567,0.038727);
#344=CIRCLE('',#4569,0.038727);
#345=CIRCLE('',#4571,0.0344270003800001);
#346=CIRCLE('',#4573,0.0344270003800001);
#347=CIRCLE('',#4578,0.014);
#348=CIRCLE('',#4581,0.014);
#349=CIRCLE('',#4583,0.01);
#595=B_SPLINE_CURVE_WITH_KNOTS('',3,(#6555,#6556,#6557,#6558,#6559,#6560,
#6561,#6562,#6563,#6564,#6565,#6566,#6567,#6568,#6569,#6570,#6571,#6572,
#6573),.UNSPECIFIED.,.T.,.F.,(1,1,1,1,1,1,1,1,1,1,1,1,1,1,1,1,1,1,1,1,1,
1,1),(-0.0118110140186832,-0.00787400934578877,-0.00393700467289439,0.,
0.00393700467289439,0.00787400934578878,0.0118110140186832,0.0157480186915776,
0.0196850233644719,0.0236220280373663,0.0275590327102607,0.0314960373831551,
0.0354330420560495,0.0393700467289439,0.0433070514018383,0.0472440560747327,
0.0511810607476271,0.0551180654205214,0.0590550700934158,0.0629920747663102,
0.0669290794392046,0.070866084112099,0.0748030887849934),.UNSPECIFIED.);
#596=B_SPLINE_CURVE_WITH_KNOTS('',3,(#6578,#6579,#6580,#6581,#6582,#6583,
#6584,#6585,#6586,#6587,#6588,#6589,#6590,#6591,#6592,#6593,#6594,#6595,
#6596,#6597,#6598),.UNSPECIFIED.,.T.,.F.,(1,1,1,1,1,1,1,1,1,1,1,1,1,1,1,
1,1,1,1,1,1,1,1,1,1),(-0.0165527839474341,-0.0110351892982894,-0.00551759464914471,
0.,0.00551759464914471,0.0110351892982894,0.0165527839474341,0.0220703785965788,
0.0275879732457236,0.0331055678948683,0.038623162544013,0.0441407571931577,
0.0496583518423024,0.0551759464914471,0.0579347438160195,0.0606935411405918,
0.0634523384651642,0.0662111357897365,0.0717287304388812,0.077246325088026,
0.0827639197371707,0.0882815143863154,0.0937991090354601,0.0993167036846048,
0.10483429833375),.UNSPECIFIED.);
#597=B_SPLINE_CURVE_WITH_KNOTS('',3,(#6604,#6605,#6606,#6607,#6608,#6609,
#6610,#6611,#6612,#6613,#6614,#6615,#6616,#6617,#6618,#6619,#6620,#6621,
#6622,#6623,#6624),.UNSPECIFIED.,.T.,.F.,(1,1,1,1,1,1,1,1,1,1,1,1,1,1,1,
1,1,1,1,1,1,1,1,1,1),(-0.0165527839474341,-0.0110351892982894,-0.00551759464914471,
0.,0.00551759464914471,0.0110351892982894,0.0165527839474341,0.0220703785965788,
0.0275879732457236,0.0331055678948683,0.038623162544013,0.0441407571931577,
0.0496583518423024,0.0551759464914471,0.0579347438160195,0.0606935411405918,
0.0634523384651642,0.0662111357897365,0.0717287304388812,0.077246325088026,
0.0827639197371707,0.0882815143863154,0.0937991090354601,0.0993167036846048,
0.10483429833375),.UNSPECIFIED.);
#598=B_SPLINE_CURVE_WITH_KNOTS('',3,(#6629,#6630,#6631,#6632,#6633,#6634,
#6635,#6636,#6637,#6638,#6639,#6640,#6641,#6642,#6643,#6644,#6645,#6646,
#6647),.UNSPECIFIED.,.T.,.F.,(1,1,1,1,1,1,1,1,1,1,1,1,1,1,1,1,1,1,1,1,1,
1,1),(-0.0118110140186832,-0.00787400934578878,-0.00393700467289439,0.,
0.00393700467289439,0.00787400934578878,0.0118110140186832,0.0157480186915776,
0.019685023364472,0.0236220280373663,0.0275590327102607,0.0314960373831551,
0.0354330420560495,0.0393700467289439,0.0433070514018383,0.0472440560747327,
0.0511810607476271,0.0551180654205215,0.0590550700934159,0.0629920747663102,
0.0669290794392046,0.070866084112099,0.0748030887849934),.UNSPECIFIED.);
#799=ORIENTED_EDGE('',*,*,#1919,.T.);
#800=ORIENTED_EDGE('',*,*,#1920,.T.);
#801=ORIENTED_EDGE('',*,*,#1921,.T.);
#802=ORIENTED_EDGE('',*,*,#1922,.T.);
#803=ORIENTED_EDGE('',*,*,#1923,.F.);
#804=ORIENTED_EDGE('',*,*,#1924,.F.);
#805=ORIENTED_EDGE('',*,*,#1925,.T.);
#806=ORIENTED_EDGE('',*,*,#1926,.F.);
#807=ORIENTED_EDGE('',*,*,#1919,.F.);
#808=ORIENTED_EDGE('',*,*,#1927,.F.);
#809=ORIENTED_EDGE('',*,*,#1928,.F.);
#810=ORIENTED_EDGE('',*,*,#1928,.T.);
#811=ORIENTED_EDGE('',*,*,#1929,.F.);
#812=ORIENTED_EDGE('',*,*,#1929,.T.);
#813=ORIENTED_EDGE('',*,*,#1930,.F.);
#814=ORIENTED_EDGE('',*,*,#1930,.T.);
#815=ORIENTED_EDGE('',*,*,#1931,.F.);
#816=ORIENTED_EDGE('',*,*,#1931,.T.);
#817=ORIENTED_EDGE('',*,*,#1932,.F.);
#818=ORIENTED_EDGE('',*,*,#1932,.T.);
#819=ORIENTED_EDGE('',*,*,#1933,.F.);
#820=ORIENTED_EDGE('',*,*,#1933,.T.);
#821=ORIENTED_EDGE('',*,*,#1934,.F.);
#822=ORIENTED_EDGE('',*,*,#1934,.T.);
#823=ORIENTED_EDGE('',*,*,#1935,.F.);
#824=ORIENTED_EDGE('',*,*,#1935,.T.);
#825=ORIENTED_EDGE('',*,*,#1936,.F.);
#826=ORIENTED_EDGE('',*,*,#1936,.T.);
#827=ORIENTED_EDGE('',*,*,#1937,.F.);
#828=ORIENTED_EDGE('',*,*,#1937,.T.);
#829=ORIENTED_EDGE('',*,*,#1938,.F.);
#830=ORIENTED_EDGE('',*,*,#1938,.T.);
#831=ORIENTED_EDGE('',*,*,#1939,.F.);
#832=ORIENTED_EDGE('',*,*,#1939,.T.);
#833=ORIENTED_EDGE('',*,*,#1940,.F.);
#834=ORIENTED_EDGE('',*,*,#1940,.T.);
#835=ORIENTED_EDGE('',*,*,#1941,.F.);
#836=ORIENTED_EDGE('',*,*,#1941,.T.);
#837=ORIENTED_EDGE('',*,*,#1942,.F.);
#838=ORIENTED_EDGE('',*,*,#1942,.T.);
#839=ORIENTED_EDGE('',*,*,#1943,.F.);
#840=ORIENTED_EDGE('',*,*,#1943,.T.);
#841=ORIENTED_EDGE('',*,*,#1922,.F.);
#842=ORIENTED_EDGE('',*,*,#1923,.T.);
#843=ORIENTED_EDGE('',*,*,#1925,.F.);
#844=ORIENTED_EDGE('',*,*,#1927,.T.);
#845=ORIENTED_EDGE('',*,*,#1921,.F.);
#846=ORIENTED_EDGE('',*,*,#1944,.T.);
#847=ORIENTED_EDGE('',*,*,#1944,.F.);
#848=ORIENTED_EDGE('',*,*,#1920,.F.);
#849=ORIENTED_EDGE('',*,*,#1924,.T.);
#850=ORIENTED_EDGE('',*,*,#1945,.F.);
#851=ORIENTED_EDGE('',*,*,#1945,.T.);
#852=ORIENTED_EDGE('',*,*,#1946,.F.);
#853=ORIENTED_EDGE('',*,*,#1926,.T.);
#854=ORIENTED_EDGE('',*,*,#1946,.T.);
#1919=EDGE_CURVE('',#2488,#2488,#595,.T.);
#1920=EDGE_CURVE('',#2489,#2489,#326,.F.);
#1921=EDGE_CURVE('',#2490,#2490,#596,.T.);
#1922=EDGE_CURVE('',#2491,#2491,#327,.T.);
#1923=EDGE_CURVE('',#2492,#2492,#328,.T.);
#1924=EDGE_CURVE('',#2493,#2493,#597,.T.);
#1925=EDGE_CURVE('',#2494,#2494,#329,.T.);
#1926=EDGE_CURVE('',#2495,#2495,#598,.T.);
#1927=EDGE_CURVE('',#2496,#2496,#330,.T.);
#1928=EDGE_CURVE('',#2497,#2497,#331,.T.);
#1929=EDGE_CURVE('',#2498,#2498,#332,.T.);
#1930=EDGE_CURVE('',#2499,#2499,#333,.T.);
#1931=EDGE_CURVE('',#2500,#2500,#334,.T.);
#1932=EDGE_CURVE('',#2501,#2501,#335,.T.);
#1933=EDGE_CURVE('',#2502,#2502,#336,.T.);
#1934=EDGE_CURVE('',#2503,#2503,#337,.T.);
#1935=EDGE_CURVE('',#2504,#2504,#338,.T.);
#1936=EDGE_CURVE('',#2505,#2505,#339,.T.);
#1937=EDGE_CURVE('',#2506,#2506,#340,.T.);
#1938=EDGE_CURVE('',#2507,#2507,#341,.T.);
#1939=EDGE_CURVE('',#2508,#2508,#342,.T.);
#1940=EDGE_CURVE('',#2509,#2509,#343,.T.);
#1941=EDGE_CURVE('',#2510,#2510,#344,.T.);
#1942=EDGE_CURVE('',#2511,#2511,#345,.T.);
#1943=EDGE_CURVE('',#2512,#2512,#346,.T.);
#1944=EDGE_CURVE('',#2513,#2513,#347,.T.);
#1945=EDGE_CURVE('',#2514,#2514,#348,.T.);
#1946=EDGE_CURVE('',#2515,#2515,#349,.T.);
#2488=VERTEX_POINT('',#6574);
#2489=VERTEX_POINT('',#6576);
#2490=VERTEX_POINT('',#6599);
#2491=VERTEX_POINT('',#6601);
#2492=VERTEX_POINT('',#6603);
#2493=VERTEX_POINT('',#6625);
#2494=VERTEX_POINT('',#6628);
#2495=VERTEX_POINT('',#6648);
#2496=VERTEX_POINT('',#6650);
#2497=VERTEX_POINT('',#6653);
#2498=VERTEX_POINT('',#6656);
#2499=VERTEX_POINT('',#6659);
#2500=VERTEX_POINT('',#6662);
#2501=VERTEX_POINT('',#6665);
#2502=VERTEX_POINT('',#6668);
#2503=VERTEX_POINT('',#6671);
#2504=VERTEX_POINT('',#6674);
#2505=VERTEX_POINT('',#6677);
#2506=VERTEX_POINT('',#6680);
#2507=VERTEX_POINT('',#6683);
#2508=VERTEX_POINT('',#6686);
#2509=VERTEX_POINT('',#6689);
#2510=VERTEX_POINT('',#6692);
#2511=VERTEX_POINT('',#6695);
#2512=VERTEX_POINT('',#6698);
#2513=VERTEX_POINT('',#6704);
#2514=VERTEX_POINT('',#6708);
#2515=VERTEX_POINT('',#6711);
#3226=EDGE_LOOP('',(#799));
#3227=EDGE_LOOP('',(#800));
#3228=EDGE_LOOP('',(#801));
#3229=EDGE_LOOP('',(#802));
#3230=EDGE_LOOP('',(#803));
#3231=EDGE_LOOP('',(#804));
#3232=EDGE_LOOP('',(#805));
#3233=EDGE_LOOP('',(#806));
#3234=EDGE_LOOP('',(#807));
#3235=EDGE_LOOP('',(#808));
#3236=EDGE_LOOP('',(#809));
#3237=EDGE_LOOP('',(#810));
#3238=EDGE_LOOP('',(#811));
#3239=EDGE_LOOP('',(#812));
#3240=EDGE_LOOP('',(#813));
#3241=EDGE_LOOP('',(#814));
#3242=EDGE_LOOP('',(#815));
#3243=EDGE_LOOP('',(#816));
#3244=EDGE_LOOP('',(#817));
#3245=EDGE_LOOP('',(#818));
#3246=EDGE_LOOP('',(#819));
#3247=EDGE_LOOP('',(#820));
#3248=EDGE_LOOP('',(#821));
#3249=EDGE_LOOP('',(#822));
#3250=EDGE_LOOP('',(#823));
#3251=EDGE_LOOP('',(#824));
#3252=EDGE_LOOP('',(#825));
#3253=EDGE_LOOP('',(#826));
#3254=EDGE_LOOP('',(#827));
#3255=EDGE_LOOP('',(#828));
#3256=EDGE_LOOP('',(#829));
#3257=EDGE_LOOP('',(#830));
#3258=EDGE_LOOP('',(#831));
#3259=EDGE_LOOP('',(#832));
#3260=EDGE_LOOP('',(#833));
#3261=EDGE_LOOP('',(#834));
#3262=EDGE_LOOP('',(#835));
#3263=EDGE_LOOP('',(#836));
#3264=EDGE_LOOP('',(#837));
#3265=EDGE_LOOP('',(#838));
#3266=EDGE_LOOP('',(#839));
#3267=EDGE_LOOP('',(#840));
#3268=EDGE_LOOP('',(#841));
#3269=EDGE_LOOP('',(#842));
#3270=EDGE_LOOP('',(#843));
#3271=EDGE_LOOP('',(#844));
#3272=EDGE_LOOP('',(#845));
#3273=EDGE_LOOP('',(#846));
#3274=EDGE_LOOP('',(#847));
#3275=EDGE_LOOP('',(#848));
#3276=EDGE_LOOP('',(#849));
#3277=EDGE_LOOP('',(#850));
#3278=EDGE_LOOP('',(#851));
#3279=EDGE_LOOP('',(#852));
#3280=EDGE_LOOP('',(#853));
#3281=EDGE_LOOP('',(#854));
#3603=FACE_BOUND('',#3226,.T.);
#3604=FACE_BOUND('',#3227,.T.);
#3605=FACE_BOUND('',#3228,.T.);
#3606=FACE_BOUND('',#3229,.T.);
#3607=FACE_BOUND('',#3230,.T.);
#3608=FACE_BOUND('',#3231,.T.);
#3609=FACE_BOUND('',#3232,.T.);
#3610=FACE_BOUND('',#3233,.T.);
#3611=FACE_BOUND('',#3234,.T.);
#3612=FACE_BOUND('',#3235,.T.);
#3613=FACE_BOUND('',#3236,.T.);
#3614=FACE_BOUND('',#3237,.T.);
#3615=FACE_BOUND('',#3238,.T.);
#3616=FACE_BOUND('',#3239,.T.);
#3617=FACE_BOUND('',#3240,.T.);
#3618=FACE_BOUND('',#3241,.T.);
#3619=FACE_BOUND('',#3242,.T.);
#3620=FACE_BOUND('',#3243,.T.);
#3621=FACE_BOUND('',#3244,.T.);
#3622=FACE_BOUND('',#3245,.T.);
#3623=FACE_BOUND('',#3246,.T.);
#3624=FACE_BOUND('',#3247,.T.);
#3625=FACE_BOUND('',#3248,.T.);
#3626=FACE_BOUND('',#3249,.T.);
#3627=FACE_BOUND('',#3250,.T.);
#3628=FACE_BOUND('',#3251,.T.);
#3629=FACE_BOUND('',#3252,.T.);
#3630=FACE_BOUND('',#3253,.T.);
#3631=FACE_BOUND('',#3254,.T.);
#3632=FACE_BOUND('',#3255,.T.);
#3633=FACE_BOUND('',#3256,.T.);
#3634=FACE_BOUND('',#3257,.T.);
#3635=FACE_BOUND('',#3258,.T.);
#3636=FACE_BOUND('',#3259,.T.);
#3637=FACE_BOUND('',#3260,.T.);
#3638=FACE_BOUND('',#3261,.T.);
#3639=FACE_BOUND('',#3262,.T.);
#3640=FACE_BOUND('',#3263,.T.);
#3641=FACE_BOUND('',#3264,.T.);
#3642=FACE_BOUND('',#3265,.T.);
#3643=FACE_BOUND('',#3266,.T.);
#3644=FACE_BOUND('',#3267,.T.);
#3645=FACE_BOUND('',#3268,.T.);
#3646=FACE_BOUND('',#3269,.T.);
#3647=FACE_BOUND('',#3270,.T.);
#3648=FACE_BOUND('',#3271,.T.);
#3649=FACE_BOUND('',#3272,.T.);
#3650=FACE_BOUND('',#3273,.T.);
#3651=FACE_BOUND('',#3274,.T.);
#3652=FACE_BOUND('',#3275,.T.);
#3653=FACE_BOUND('',#3276,.T.);
#3654=FACE_BOUND('',#3277,.T.);
#3655=FACE_BOUND('',#3278,.T.);
#3656=FACE_BOUND('',#3279,.T.);
#3657=FACE_BOUND('',#3280,.T.);
#3658=FACE_BOUND('',#3281,.T.);
#3959=PLANE('',#4542);
#3960=PLANE('',#4546);
#3961=PLANE('',#4550);
#3962=PLANE('',#4554);
#3963=PLANE('',#4558);
#3964=PLANE('',#4562);
#3965=PLANE('',#4566);
#3966=PLANE('',#4570);
#3967=PLANE('',#4574);
#3968=PLANE('',#4575);
#3969=PLANE('',#4576);
#3970=PLANE('',#4579);
#3971=PLANE('',#4582);
#4064=ADVANCED_FACE('',(#3603,#3604),#209,.F.);
#4065=ADVANCED_FACE('',(#3605,#3606,#3607,#3608),#210,.T.);
#4066=ADVANCED_FACE('',(#3609,#3610,#3611,#3612),#211,.F.);
#4067=ADVANCED_FACE('',(#3613),#3959,.T.);
#4068=ADVANCED_FACE('',(#3614,#3615),#212,.T.);
#4069=ADVANCED_FACE('',(#3616,#3617),#3960,.T.);
#4070=ADVANCED_FACE('',(#3618,#3619),#213,.T.);
#4071=ADVANCED_FACE('',(#3620,#3621),#3961,.T.);
#4072=ADVANCED_FACE('',(#3622,#3623),#214,.T.);
#4073=ADVANCED_FACE('',(#3624,#3625),#3962,.T.);
#4074=ADVANCED_FACE('',(#3626,#3627),#215,.T.);
#4075=ADVANCED_FACE('',(#3628,#3629),#3963,.T.);
#4076=ADVANCED_FACE('',(#3630,#3631),#216,.T.);
#4077=ADVANCED_FACE('',(#3632,#3633),#3964,.T.);
#4078=ADVANCED_FACE('',(#3634,#3635),#217,.T.);
#4079=ADVANCED_FACE('',(#3636,#3637),#3965,.T.);
#4080=ADVANCED_FACE('',(#3638,#3639),#218,.T.);
#4081=ADVANCED_FACE('',(#3640,#3641),#3966,.T.);
#4082=ADVANCED_FACE('',(#3642,#3643),#219,.T.);
#4083=ADVANCED_FACE('',(#3644,#3645),#3967,.T.);
#4084=ADVANCED_FACE('',(#3646,#3647),#3968,.T.);
#4085=ADVANCED_FACE('',(#3648),#3969,.T.);
#4086=ADVANCED_FACE('',(#3649,#3650),#220,.F.);
#4087=ADVANCED_FACE('',(#3651,#3652),#3970,.F.);
#4088=ADVANCED_FACE('',(#3653,#3654),#221,.F.);
#4089=ADVANCED_FACE('',(#3655,#3656),#3971,.F.);
#4090=ADVANCED_FACE('',(#3657,#3658),#222,.F.);
#4326=CLOSED_SHELL('',(#4064,#4065,#4066,#4067,#4068,#4069,#4070,#4071,
#4072,#4073,#4074,#4075,#4076,#4077,#4078,#4079,#4080,#4081,#4082,#4083,
#4084,#4085,#4086,#4087,#4088,#4089,#4090));
#4337=STYLED_ITEM('',(#4348),#4452);
#4348=PRESENTATION_STYLE_ASSIGNMENT((#4364));
#4364=SURFACE_STYLE_USAGE(.BOTH.,#4380);
#4380=SURFACE_SIDE_STYLE('',(#4396));
#4396=SURFACE_STYLE_FILL_AREA(#4412);
#4412=FILL_AREA_STYLE('',(#4428));
#4428=FILL_AREA_STYLE_COLOUR('',#4444);
#4444=COLOUR_RGB('', 0.72549020, 0.75294118, 0.79215686);
#4452=MANIFOLD_SOLID_BREP('Part 1',#4326);
#4464=SHAPE_DEFINITION_REPRESENTATION(#8569,#4476);
#4476=SHAPE_REPRESENTATION('Part 1',(#4484),#8539);
#4484=AXIS2_PLACEMENT_3D('',#6402,#5064,#5065);
#4534=AXIS2_PLACEMENT_3D('',#6554,#5184,#5185);
#4535=AXIS2_PLACEMENT_3D('',#6575,#5186,#5187);
#4536=AXIS2_PLACEMENT_3D('',#6577,#5188,#5189);
#4537=AXIS2_PLACEMENT_3D('',#6600,#5190,#5191);
#4538=AXIS2_PLACEMENT_3D('',#6602,#5192,#5193);
#4539=AXIS2_PLACEMENT_3D('',#6626,#5194,#5195);
#4540=AXIS2_PLACEMENT_3D('',#6627,#5196,#5197);
#4541=AXIS2_PLACEMENT_3D('',#6649,#5198,#5199);
#4542=AXIS2_PLACEMENT_3D('',#6651,#5200,#5201);
#4543=AXIS2_PLACEMENT_3D('',#6652,#5202,#5203);
#4544=AXIS2_PLACEMENT_3D('',#6654,#5204,#5205);
#4545=AXIS2_PLACEMENT_3D('',#6655,#5206,#5207);
#4546=AXIS2_PLACEMENT_3D('',#6657,#5208,#5209);
#4547=AXIS2_PLACEMENT_3D('',#6658,#5210,#5211);
#4548=AXIS2_PLACEMENT_3D('',#6660,#5212,#5213);
#4549=AXIS2_PLACEMENT_3D('',#6661,#5214,#5215);
#4550=AXIS2_PLACEMENT_3D('',#6663,#5216,#5217);
#4551=AXIS2_PLACEMENT_3D('',#6664,#5218,#5219);
#4552=AXIS2_PLACEMENT_3D('',#6666,#5220,#5221);
#4553=AXIS2_PLACEMENT_3D('',#6667,#5222,#5223);
#4554=AXIS2_PLACEMENT_3D('',#6669,#5224,#5225);
#4555=AXIS2_PLACEMENT_3D('',#6670,#5226,#5227);
#4556=AXIS2_PLACEMENT_3D('',#6672,#5228,#5229);
#4557=AXIS2_PLACEMENT_3D('',#6673,#5230,#5231);
#4558=AXIS2_PLACEMENT_3D('',#6675,#5232,#5233);
#4559=AXIS2_PLACEMENT_3D('',#6676,#5234,#5235);
#4560=AXIS2_PLACEMENT_3D('',#6678,#5236,#5237);
#4561=AXIS2_PLACEMENT_3D('',#6679,#5238,#5239);
#4562=AXIS2_PLACEMENT_3D('',#6681,#5240,#5241);
#4563=AXIS2_PLACEMENT_3D('',#6682,#5242,#5243);
#4564=AXIS2_PLACEMENT_3D('',#6684,#5244,#5245);
#4565=AXIS2_PLACEMENT_3D('',#6685,#5246,#5247);
#4566=AXIS2_PLACEMENT_3D('',#6687,#5248,#5249);
#4567=AXIS2_PLACEMENT_3D('',#6688,#5250,#5251);
#4568=AXIS2_PLACEMENT_3D('',#6690,#5252,#5253);
#4569=AXIS2_PLACEMENT_3D('',#6691,#5254,#5255);
#4570=AXIS2_PLACEMENT_3D('',#6693,#5256,#5257);
#4571=AXIS2_PLACEMENT_3D('',#6694,#5258,#5259);
#4572=AXIS2_PLACEMENT_3D('',#6696,#5260,#5261);
#4573=AXIS2_PLACEMENT_3D('',#6697,#5262,#5263);
#4574=AXIS2_PLACEMENT_3D('',#6699,#5264,#5265);
#4575=AXIS2_PLACEMENT_3D('',#6700,#5266,#5267);
#4576=AXIS2_PLACEMENT_3D('',#6701,#5268,#5269);
#4577=AXIS2_PLACEMENT_3D('',#6702,#5270,#5271);
#4578=AXIS2_PLACEMENT_3D('',#6703,#5272,#5273);
#4579=AXIS2_PLACEMENT_3D('',#6705,#5274,#5275);
#4580=AXIS2_PLACEMENT_3D('',#6706,#5276,#5277);
#4581=AXIS2_PLACEMENT_3D('',#6707,#5278,#5279);
#4582=AXIS2_PLACEMENT_3D('',#6709,#5280,#5281);
#4583=AXIS2_PLACEMENT_3D('',#6710,#5282,#5283);
#4584=AXIS2_PLACEMENT_3D('',#6712,#5284,#5285);
#5064=DIRECTION('',(0.,0.,1.));
#5065=DIRECTION('',(1.,0.,0.));
#5184=DIRECTION('',(0.,0.,1.));
#5185=DIRECTION('',(1.,0.,0.));
#5186=DIRECTION('',(0.,0.,1.));
#5187=DIRECTION('',(1.,0.,0.));
#5188=DIRECTION('',(1.82918119333769E-16,-1.,0.));
#5189=DIRECTION('',(1.,1.82918119333769E-16,0.));
#5190=DIRECTION('',(1.82918119333769E-16,-1.,0.));
#5191=DIRECTION('',(1.,1.82918119333769E-16,0.));
#5192=DIRECTION('',(1.82918119333769E-16,-1.,0.));
#5193=DIRECTION('',(1.,1.82918119333769E-16,0.));
#5194=DIRECTION('',(1.82918119333769E-16,-1.,0.));
#5195=DIRECTION('',(1.,1.82918119333769E-16,0.));
#5196=DIRECTION('',(1.82918119333769E-16,-1.,0.));
#5197=DIRECTION('',(1.,1.82918119333769E-16,0.));
#5198=DIRECTION('',(1.82918119333769E-16,-1.,0.));
#5199=DIRECTION('',(1.,1.82918119333769E-16,0.));
#5200=DIRECTION('',(-1.82918119333769E-16,1.,0.));
#5201=DIRECTION('',(-1.,-1.82918119333769E-16,0.));
#5202=DIRECTION('',(1.82918119333769E-16,-1.,0.));
#5203=DIRECTION('',(1.,1.82918119333769E-16,0.));
#5204=DIRECTION('',(1.82918119333769E-16,-1.,0.));
#5205=DIRECTION('',(1.,1.82918119333769E-16,0.));
#5206=DIRECTION('',(1.82918119333769E-16,-1.,0.));
#5207=DIRECTION('',(1.,1.82918119333769E-16,0.));
#5208=DIRECTION('',(1.82918119333769E-16,-1.,0.));
#5209=DIRECTION('',(1.,1.82918119333769E-16,0.));
#5210=DIRECTION('',(1.82918119333769E-16,-1.,0.));
#5211=DIRECTION('',(1.,1.82918119333769E-16,0.));
#5212=DIRECTION('',(1.82918119333769E-16,-1.,0.));
#5213=DIRECTION('',(1.,1.82918119333769E-16,0.));
#5214=DIRECTION('',(1.82918119333769E-16,-1.,0.));
#5215=DIRECTION('',(1.,1.82918119333769E-16,0.));
#5216=DIRECTION('',(-1.82918119333769E-16,1.,0.));
#5217=DIRECTION('',(-1.,-1.82918119333769E-16,0.));
#5218=DIRECTION('',(1.82918119333769E-16,-1.,0.));
#5219=DIRECTION('',(1.,1.82918119333769E-16,0.));
#5220=DIRECTION('',(1.82918119333769E-16,-1.,0.));
#5221=DIRECTION('',(1.,1.82918119333769E-16,0.));
#5222=DIRECTION('',(1.82918119333769E-16,-1.,0.));
#5223=DIRECTION('',(1.,1.82918119333769E-16,0.));
#5224=DIRECTION('',(1.82918119333769E-16,-1.,0.));
#5225=DIRECTION('',(1.,1.82918119333769E-16,0.));
#5226=DIRECTION('',(1.82918119333769E-16,-1.,0.));
#5227=DIRECTION('',(1.,1.82918119333769E-16,0.));
#5228=DIRECTION('',(1.82918119333769E-16,-1.,0.));
#5229=DIRECTION('',(1.,1.82918119333769E-16,0.));
#5230=DIRECTION('',(1.82918119333769E-16,-1.,0.));
#5231=DIRECTION('',(1.,1.82918119333769E-16,0.));
#5232=DIRECTION('',(-1.82918119333769E-16,1.,0.));
#5233=DIRECTION('',(-1.,-1.82918119333769E-16,0.));
#5234=DIRECTION('',(1.82918119333769E-16,-1.,0.));
#5235=DIRECTION('',(1.,1.82918119333769E-16,0.));
#5236=DIRECTION('',(1.82918119333769E-16,-1.,0.));
#5237=DIRECTION('',(1.,1.82918119333769E-16,0.));
#5238=DIRECTION('',(1.82918119333769E-16,-1.,0.));
#5239=DIRECTION('',(1.,1.82918119333769E-16,0.));
#5240=DIRECTION('',(1.82918119333769E-16,-1.,0.));
#5241=DIRECTION('',(1.,1.82918119333769E-16,0.));
#5242=DIRECTION('',(1.82918119333769E-16,-1.,0.));
#5243=DIRECTION('',(1.,1.82918119333769E-16,0.));
#5244=DIRECTION('',(1.82918119333769E-16,-1.,0.));
#5245=DIRECTION('',(1.,1.82918119333769E-16,0.));
#5246=DIRECTION('',(1.82918119333769E-16,-1.,0.));
#5247=DIRECTION('',(1.,1.82918119333769E-16,0.));
#5248=DIRECTION('',(-1.82918119333769E-16,1.,0.));
#5249=DIRECTION('',(-1.,-1.82918119333769E-16,0.));
#5250=DIRECTION('',(1.82918119333769E-16,-1.,0.));
#5251=DIRECTION('',(1.,1.82918119333769E-16,0.));
#5252=DIRECTION('',(1.82918119333769E-16,-1.,0.));
#5253=DIRECTION('',(1.,1.82918119333769E-16,0.));
#5254=DIRECTION('',(1.82918119333769E-16,-1.,0.));
#5255=DIRECTION('',(1.,1.82918119333769E-16,0.));
#5256=DIRECTION('',(1.82918119333769E-16,-1.,0.));
#5257=DIRECTION('',(1.,1.82918119333769E-16,0.));
#5258=DIRECTION('',(1.82918119333769E-16,-1.,0.));
#5259=DIRECTION('',(1.,1.82918119333769E-16,0.));
#5260=DIRECTION('',(1.82918119333769E-16,-1.,0.));
#5261=DIRECTION('',(1.,1.82918119333769E-16,0.));
#5262=DIRECTION('',(1.82918119333769E-16,-1.,0.));
#5263=DIRECTION('',(1.,1.82918119333769E-16,0.));
#5264=DIRECTION('',(-1.82918119333769E-16,1.,0.));
#5265=DIRECTION('',(-1.,-1.82918119333769E-16,0.));
#5266=DIRECTION('',(1.82918119333769E-16,-1.,0.));
#5267=DIRECTION('',(1.,1.82918119333769E-16,0.));
#5268=DIRECTION('',(1.82918119333769E-16,-1.,0.));
#5269=DIRECTION('',(1.,1.82918119333769E-16,0.));
#5270=DIRECTION('',(0.,0.,-1.));
#5271=DIRECTION('',(-1.,0.,0.));
#5272=DIRECTION('',(0.,0.,1.));
#5273=DIRECTION('',(1.,0.,0.));
#5274=DIRECTION('',(0.,0.,1.));
#5275=DIRECTION('',(1.,0.,0.));
#5276=DIRECTION('',(0.,0.,1.));
#5277=DIRECTION('',(-1.,0.,0.));
#5278=DIRECTION('',(0.,0.,1.));
#5279=DIRECTION('',(1.,0.,0.));
#5280=DIRECTION('',(0.,0.,-1.));
#5281=DIRECTION('',(1.,0.,0.));
#5282=DIRECTION('',(0.,0.,1.));
#5283=DIRECTION('',(1.,0.,0.));
#5284=DIRECTION('',(0.,0.,1.));
#5285=DIRECTION('',(1.,0.,0.));
#6402=CARTESIAN_POINT('',(0.,0.,0.));
#6554=CARTESIAN_POINT('',(6.93889390390723E-18,-0.01000000007,-0.03408));
#6555=CARTESIAN_POINT('',(0.00946663159093614,-0.0139561679473873,-0.0278767736634555));
#6556=CARTESIAN_POINT('',(0.0102666200478305,-0.0100000565954907,-0.0275752828436828));
#6557=CARTESIAN_POINT('',(0.00946688821774168,-0.00604360609065003,-0.0278767285229424));
#6558=CARTESIAN_POINT('',(0.00725035830735357,-0.00274839440570845,-0.0285683176118653));
#6559=CARTESIAN_POINT('',(0.00395507415494214,-0.00053339877994205,-0.0292396064107534));
#6560=CARTESIAN_POINT('',(8.7295912523717E-6,0.000265578825293647,-0.0295203456594297));
#6561=CARTESIAN_POINT('',(-0.00395003344396799,-0.000528930247298576,-0.0292410106298082));
#6562=CARTESIAN_POINT('',(-0.00725619049089152,-0.00275303181564925,-0.0285668891854122));
#6563=CARTESIAN_POINT('',(-0.00946785242770053,-0.00604878322242755,-0.0278762714324907));
#6564=CARTESIAN_POINT('',(-0.010265338281535,-0.00999489822950936,-0.0275757620013937));
#6565=CARTESIAN_POINT('',(-0.00947078950931377,-0.0139472845698404,-0.0278753159068785));
#6566=CARTESIAN_POINT('',(-0.00725435049491199,-0.0172490827823861,-0.0285674371250356));
#6567=CARTESIAN_POINT('',(-0.00395206613480992,-0.0194689363159613,-0.0292403663038441));
#6568=CARTESIAN_POINT('',(-3.96206978751156E-7,-0.0202655823062788,-0.029520344557746));
#6569=CARTESIAN_POINT('',(0.00395294398365647,-0.0194687348747586,-0.0292402596637565));
#6570=CARTESIAN_POINT('',(0.00725259756702223,-0.0172494862997466,-0.0285677364036141));
#6571=CARTESIAN_POINT('',(0.00946663159093614,-0.0139561679473873,-0.0278767736634555));
#6572=CARTESIAN_POINT('',(0.0102666200478305,-0.0100000565954907,-0.0275752828436828));
#6573=CARTESIAN_POINT('',(0.00946688821774168,-0.00604360609065003,-0.0278767285229424));
#6574=CARTESIAN_POINT('',(0.01,-0.01000000007,-0.0276757722601882));
#6575=CARTESIAN_POINT('',(6.93889390390723E-18,-0.01000000007,-0.034078));
#6576=CARTESIAN_POINT('',(0.01,-0.01000000007,-0.034078));
#6577=CARTESIAN_POINT('',(0.,-0.0569016393442623,0.));
#6578=CARTESIAN_POINT('',(-0.0132533893149118,-0.00446383140324631,-0.0364099611309221));
#6579=CARTESIAN_POINT('',(-0.0143737540409632,-0.00999787707861307,-0.0359566639800123));
#6580=CARTESIAN_POINT('',(-0.0132515945212353,-0.0155446607023014,-0.0364107901432995));
#6581=CARTESIAN_POINT('',(-0.0101500584303514,-0.0201510160446614,-0.0374462176304152));
#6582=CARTESIAN_POINT('',(-0.00554229810874566,-0.0232510882909091,-0.0384472488580326));
#6583=CARTESIAN_POINT('',(-1.26629420446097E-5,-0.0243729960180894,-0.0388663870917174));
#6584=CARTESIAN_POINT('',(0.00553690033500876,-0.023256909357022,-0.0384491960150612));
#6585=CARTESIAN_POINT('',(0.0101593273036987,-0.0201434215672515,-0.0374437158522921));
#6586=CARTESIAN_POINT('',(0.0132531589529878,-0.0155359599646523,-0.0364100584582362));
#6587=CARTESIAN_POINT('',(0.0143721784014614,-0.0100067959764106,-0.0359571541294907));
#6588=CARTESIAN_POINT('',(0.0132581215780687,-0.00446824126569558,-0.0364087344913512));
#6589=CARTESIAN_POINT('',(0.010666489619777,-0.00061724692514208,-0.0372730694062662));
#6590=CARTESIAN_POINT('',(0.00785058238386626,0.00169977372296183,-0.0379469071648758));
#6591=CARTESIAN_POINT('',(0.00541380149881201,0.00300821979624252,-0.0383754503653669));
#6592=CARTESIAN_POINT('',(0.00278404945627228,0.0038132451617009,-0.0386587997617237));
#6593=CARTESIAN_POINT('',(-0.000935274336576486,0.00418676378220625,-0.0387958699540579));
#6594=CARTESIAN_POINT('',(-0.00553839643887497,0.00325289608103151,-0.0384481705128959));
#6595=CARTESIAN_POINT('',(-0.0101574153340434,0.000145854240069477,-0.0374443881689455));
#6596=CARTESIAN_POINT('',(-0.0132533893149118,-0.00446383140324631,-0.0364099611309221));
#6597=CARTESIAN_POINT('',(-0.0143737540409632,-0.00999787707861307,-0.0359566639800123));
#6598=CARTESIAN_POINT('',(-0.0132515945212353,-0.0155446607023014,-0.0364107901432995));
#6599=CARTESIAN_POINT('',(-0.014,-0.01000000007,-0.0361079011990451));
#6600=CARTESIAN_POINT('',(-1.30606535733962E-17,0.01449999993,0.));
#6601=CARTESIAN_POINT('',(0.038727,0.01449999993,0.));
#6602=CARTESIAN_POINT('',(-2.35994359237075E-18,-0.04400000007,0.));
#6603=CARTESIAN_POINT('',(0.038727,-0.04400000007,0.));
#6604=CARTESIAN_POINT('',(-0.0132533893149118,-0.00446383140324631,0.0364099611309221));
#6605=CARTESIAN_POINT('',(-0.0143737540409632,-0.00999787707861307,0.0359566639800123));
#6606=CARTESIAN_POINT('',(-0.0132515945212353,-0.0155446607023014,0.0364107901432995));
#6607=CARTESIAN_POINT('',(-0.0101500584303514,-0.0201510160446614,0.0374462176304152));
#6608=CARTESIAN_POINT('',(-0.00554229810874566,-0.0232510882909091,0.0384472488580326));
#6609=CARTESIAN_POINT('',(-1.26629420446097E-5,-0.0243729960180894,0.0388663870917174));
#6610=CARTESIAN_POINT('',(0.00553690033500876,-0.023256909357022,0.0384491960150612));
#6611=CARTESIAN_POINT('',(0.0101593273036987,-0.0201434215672515,0.0374437158522921));
#6612=CARTESIAN_POINT('',(0.0132531589529878,-0.0155359599646523,0.0364100584582362));
#6613=CARTESIAN_POINT('',(0.0143721784014614,-0.0100067959764106,0.0359571541294907));
#6614=CARTESIAN_POINT('',(0.0132581215780687,-0.00446824126569558,0.0364087344913512));
#6615=CARTESIAN_POINT('',(0.010666489619777,-0.00061724692514208,0.0372730694062662));
#6616=CARTESIAN_POINT('',(0.00785058238386626,0.00169977372296183,0.0379469071648758));
#6617=CARTESIAN_POINT('',(0.00541380149881201,0.00300821979624252,0.0383754503653669));
#6618=CARTESIAN_POINT('',(0.00278404945627228,0.0038132451617009,0.0386587997617237));
#6619=CARTESIAN_POINT('',(-0.000935274336576486,0.00418676378220625,0.0387958699540579));
#6620=CARTESIAN_POINT('',(-0.00553839643887497,0.00325289608103151,0.0384481705128959));
#6621=CARTESIAN_POINT('',(-0.0101574153340434,0.000145854240069477,0.0374443881689455));
#6622=CARTESIAN_POINT('',(-0.0132533893149118,-0.00446383140324631,0.0364099611309221));
#6623=CARTESIAN_POINT('',(-0.0143737540409632,-0.00999787707861307,0.0359566639800123));
#6624=CARTESIAN_POINT('',(-0.0132515945212353,-0.0155446607023014,0.0364107901432995));
#6625=CARTESIAN_POINT('',(-0.014,-0.01000000007,0.0361079011990451));
#6626=CARTESIAN_POINT('',(0.,-0.0569016393442623,0.));
#6627=CARTESIAN_POINT('',(-2.35994359237075E-18,-0.04400000007,0.));
#6628=CARTESIAN_POINT('',(0.0294270007,-0.04400000007,0.));
#6629=CARTESIAN_POINT('',(0.00946663159093613,-0.00604383219261268,0.0278767736634555));
#6630=CARTESIAN_POINT('',(0.0102666200478305,-0.00999994354450934,0.0275752828436828));
#6631=CARTESIAN_POINT('',(0.00946688821774168,-0.01395639404935,0.0278767285229424));
#6632=CARTESIAN_POINT('',(0.00725035830735357,-0.0172516057342916,0.0285683176118653));
#6633=CARTESIAN_POINT('',(0.00395507415494213,-0.019466601360058,0.0292396064107534));
#6634=CARTESIAN_POINT('',(8.72959125237468E-6,-0.0202655789652937,0.0295203456594297));
#6635=CARTESIAN_POINT('',(-0.00395003344396804,-0.0194710698927014,0.0292410106298082));
#6636=CARTESIAN_POINT('',(-0.0072561904908915,-0.0172469683243508,0.0285668891854122));
#6637=CARTESIAN_POINT('',(-0.00946785242770053,-0.0139512169175724,0.0278762714324907));
#6638=CARTESIAN_POINT('',(-0.010265338281535,-0.0100051019104906,0.0275757620013937));
#6639=CARTESIAN_POINT('',(-0.00947078950931378,-0.00605271557015959,0.0278753159068785));
#6640=CARTESIAN_POINT('',(-0.00725435049491192,-0.00275091735761384,0.0285674371250356));
#6641=CARTESIAN_POINT('',(-0.00395206613480994,-0.000531063824038759,0.0292403663038441));
#6642=CARTESIAN_POINT('',(-3.96206978744596E-7,0.000265582166278759,0.029520344557746));
#6643=CARTESIAN_POINT('',(0.00395294398365648,-0.000531265265241394,0.0292402596637565));
#6644=CARTESIAN_POINT('',(0.00725259756702223,-0.00275051384025345,0.0285677364036141));
#6645=CARTESIAN_POINT('',(0.00946663159093613,-0.00604383219261268,0.0278767736634555));
#6646=CARTESIAN_POINT('',(0.0102666200478305,-0.00999994354450934,0.0275752828436828));
#6647=CARTESIAN_POINT('',(0.00946688821774168,-0.01395639404935,0.0278767285229424));
#6648=CARTESIAN_POINT('',(0.01,-0.01000000007,0.0276757722601882));
#6649=CARTESIAN_POINT('',(-1.70848528828529E-17,0.03650000367,0.));
#6650=CARTESIAN_POINT('',(0.0294270007,0.03650000367,0.));
#6651=CARTESIAN_POINT('',(6.47884089682804E-34,0.04400000007,0.));
#6652=CARTESIAN_POINT('',(-1.84567381193509E-17,0.04400000007,0.));
#6653=CARTESIAN_POINT('',(0.038727,0.04400000007,0.));
#6654=CARTESIAN_POINT('',(0.,-0.0569016393442623,0.));
#6655=CARTESIAN_POINT('',(-1.70299767885476E-17,0.03620000007,0.));
#6656=CARTESIAN_POINT('',(0.038727,0.03620000007,0.));
#6657=CARTESIAN_POINT('',(0.038727,0.03620000007,0.));
#6658=CARTESIAN_POINT('',(-1.70299767885476E-17,0.03620000007,0.));
#6659=CARTESIAN_POINT('',(0.03442700038,0.03620000007,0.));
#6660=CARTESIAN_POINT('',(0.,-0.0569016393442623,0.));
#6661=CARTESIAN_POINT('',(-1.64812224305462E-17,0.03320000007,0.));
#6662=CARTESIAN_POINT('',(0.03442700038,0.03320000007,0.));
#6663=CARTESIAN_POINT('',(0.03442700038,0.03320000007,0.));
#6664=CARTESIAN_POINT('',(-1.64812224305462E-17,0.03320000007,0.));
#6665=CARTESIAN_POINT('',(0.038727,0.03320000007,0.));
#6666=CARTESIAN_POINT('',(0.,-0.0569016393442623,0.));
#6667=CARTESIAN_POINT('',(-1.58958844633116E-17,0.03000000015,0.));
#6668=CARTESIAN_POINT('',(0.038727,0.03000000015,0.));
#6669=CARTESIAN_POINT('',(0.038727,0.03000000015,0.));
#6670=CARTESIAN_POINT('',(-1.58958844633116E-17,0.03000000015,0.));
#6671=CARTESIAN_POINT('',(0.03442700038,0.03000000015,0.));
#6672=CARTESIAN_POINT('',(0.,-0.0569016393442623,0.));
#6673=CARTESIAN_POINT('',(-1.53471301053103E-17,0.02700000015,0.));
#6674=CARTESIAN_POINT('',(0.03442700038,0.02700000015,0.));
#6675=CARTESIAN_POINT('',(0.03442700038,0.02700000015,0.));
#6676=CARTESIAN_POINT('',(-1.53471301053103E-17,0.0270000001499999,0.));
#6677=CARTESIAN_POINT('',(0.038727,0.02700000015,0.));
#6678=CARTESIAN_POINT('',(0.,-0.0569016393442623,0.));
#6679=CARTESIAN_POINT('',(-1.47617921380757E-17,0.02380000023,0.));
#6680=CARTESIAN_POINT('',(0.038727,0.02380000023,0.));
#6681=CARTESIAN_POINT('',(0.038727,0.02380000023,0.));
#6682=CARTESIAN_POINT('',(-1.47617921380757E-17,0.02380000023,0.));
#6683=CARTESIAN_POINT('',(0.03442700038,0.02380000023,0.));
#6684=CARTESIAN_POINT('',(0.,-0.0569016393442623,0.));
#6685=CARTESIAN_POINT('',(-1.42130377800744E-17,0.02080000023,0.));
#6686=CARTESIAN_POINT('',(0.03442700038,0.02080000023,0.));
#6687=CARTESIAN_POINT('',(0.03442700038,0.02080000023,0.));
#6688=CARTESIAN_POINT('',(-1.42130377800744E-17,0.0208000002299999,0.));
#6689=CARTESIAN_POINT('',(0.038727,0.02080000023,0.));
#6690=CARTESIAN_POINT('',(0.,-0.0569016393442623,0.));
#6691=CARTESIAN_POINT('',(-1.36276998128398E-17,0.01760000031,0.));
#6692=CARTESIAN_POINT('',(0.038727,0.01760000031,0.));
#6693=CARTESIAN_POINT('',(0.038727,0.01760000031,0.));
#6694=CARTESIAN_POINT('',(-1.36276998128398E-17,0.01760000031,0.));
#6695=CARTESIAN_POINT('',(0.03442700038,0.01760000031,0.));
#6696=CARTESIAN_POINT('',(0.,-0.0569016393442623,0.));
#6697=CARTESIAN_POINT('',(-1.30606535733962E-17,0.01449999993,0.));
#6698=CARTESIAN_POINT('',(0.03442700038,0.01449999993,0.));
#6699=CARTESIAN_POINT('',(0.03442700038,0.01449999993,0.));
#6700=CARTESIAN_POINT('',(0.038727,-0.04400000007,0.));
#6701=CARTESIAN_POINT('',(0.0294270007,0.03650000367,0.));
#6702=CARTESIAN_POINT('',(6.93889390390723E-18,-0.01000000007,-0.034078));
#6703=CARTESIAN_POINT('',(6.93889390390723E-18,-0.01000000007,-0.034078));
#6704=CARTESIAN_POINT('',(0.014,-0.01000000007,-0.034078));
#6705=CARTESIAN_POINT('',(6.93889390390723E-18,-0.01000000007,-0.034078));
#6706=CARTESIAN_POINT('',(6.93889390390723E-18,-0.01000000007,0.034078));
#6707=CARTESIAN_POINT('',(6.93889390390723E-18,-0.01000000007,0.034078));
#6708=CARTESIAN_POINT('',(0.014,-0.01000000007,0.034078));
#6709=CARTESIAN_POINT('',(6.93889390390723E-18,-0.01000000007,0.034078));
#6710=CARTESIAN_POINT('',(6.93889390390723E-18,-0.01000000007,0.034078));
#6711=CARTESIAN_POINT('',(0.01,-0.01000000007,0.034078));
#6712=CARTESIAN_POINT('',(6.93889390390723E-18,-0.01000000007,-0.03408));
#8534=MECHANICAL_DESIGN_GEOMETRIC_PRESENTATION_REPRESENTATION('',(#4337),#8535);
#8535=(
GEOMETRIC_REPRESENTATION_CONTEXT(3)
GLOBAL_UNCERTAINTY_ASSIGNED_CONTEXT((#8547))
GLOBAL_UNIT_ASSIGNED_CONTEXT((#8561,#8560,#8559))
REPRESENTATION_CONTEXT('MAS-680','TOP_LEVEL_ASSEMBLY_PART')
);
#8539=(
GEOMETRIC_REPRESENTATION_CONTEXT(3)
GLOBAL_UNCERTAINTY_ASSIGNED_CONTEXT((#8551))
GLOBAL_UNIT_ASSIGNED_CONTEXT((#8561,#8560,#8559))
REPRESENTATION_CONTEXT('Part 1','COMPONENT_PART')
);
#8547=UNCERTAINTY_MEASURE_WITH_UNIT(LENGTH_MEASURE(1.E-8),#8561,
'DISTANCE_ACCURACY_VALUE','Maximum Tolerance applied to model');
#8551=UNCERTAINTY_MEASURE_WITH_UNIT(LENGTH_MEASURE(2.E-5),#8561,
'DISTANCE_ACCURACY_VALUE','Maximum Tolerance applied to model');
#8559=(
NAMED_UNIT(*)
SI_UNIT($,.STERADIAN.)
SOLID_ANGLE_UNIT()
);
#8560=(
NAMED_UNIT(*)
PLANE_ANGLE_UNIT()
SI_UNIT($,.RADIAN.)
);
#8561=(
LENGTH_UNIT()
NAMED_UNIT(*)
SI_UNIT($,.METRE.)
);
#8569=PRODUCT_DEFINITION_SHAPE('','',#8593);
#8593=PRODUCT_DEFINITION('','',#8617,#8605);
#8605=PRODUCT_DEFINITION_CONTEXT('',#8674,'design');
#8617=PRODUCT_DEFINITION_FORMATION_WITH_SPECIFIED_SOURCE('','',#8641,
 .NOT_KNOWN.);
#8641=PRODUCT('Part 1','Part 1','Part 1',(#8665));
#8665=PRODUCT_CONTEXT('',#8674,'mechanical');
#8674=APPLICATION_CONTEXT('managed model based 3d engineering');
ENDSEC;
END-ISO-10303-21;
